ISO-10303-21;
HEADER;
/* Generated by software containing ST-Developer
 * from STEP Tools, Inc. (www.steptools.com) 
 */

FILE_DESCRIPTION(
/* description */ ('Bin tilter linkage'),
/* implementation_level */ '2;1');

FILE_NAME(
/* name */ 'Bearing cap (1).step',
/* time_stamp */ '2026-10-28T03:26:24-07:00',
/* author */ (''),
/* organization */ (''),
/* preprocessor_version */ 'ST-DEVELOPER v20.2',
/* originating_system */ 'Autodesk Translation Framework v15.17.0.0',
/* authorisation */ '');

FILE_SCHEMA (('AUTOMOTIVE_DESIGN { 1 0 10303 214 3 1 1 }'));
ENDSEC;

DATA;
#10=MECHANICAL_DESIGN_GEOMETRIC_PRESENTATION_REPRESENTATION('',(#898),#23728);
#686=SHAPE_REPRESENTATION_RELATIONSHIP('SRR','None',#24151,#792);
#792=ADVANCED_BREP_SHAPE_REPRESENTATION('',(#1011),#23651);
#898=STYLED_ITEM('',(#24765),#1011);
#1011=MANIFOLD_SOLID_BREP('Body1',#12429);
#1268=FACE_BOUND('',#3148,.T.);
#1269=FACE_BOUND('',#3149,.T.);
#1270=FACE_BOUND('',#3150,.T.);
#1271=FACE_BOUND('',#3151,.T.);
#1272=FACE_BOUND('',#3152,.T.);
#1273=FACE_BOUND('',#3154,.T.);
#1274=FACE_BOUND('',#3155,.T.);
#1275=FACE_BOUND('',#3156,.T.);
#1276=FACE_BOUND('',#3157,.T.);
#1277=FACE_BOUND('',#3158,.T.);
#1635=PLANE('',#14323);
#1636=PLANE('',#14324);
#2183=FACE_OUTER_BOUND('',#3141,.T.);
#2184=FACE_OUTER_BOUND('',#3142,.T.);
#2185=FACE_OUTER_BOUND('',#3143,.T.);
#2186=FACE_OUTER_BOUND('',#3144,.T.);
#2187=FACE_OUTER_BOUND('',#3145,.T.);
#2188=FACE_OUTER_BOUND('',#3146,.T.);
#2189=FACE_OUTER_BOUND('',#3147,.T.);
#2190=FACE_OUTER_BOUND('',#3153,.T.);
#3141=EDGE_LOOP('',(#9541,#9542,#9543,#9544));
#3142=EDGE_LOOP('',(#9545,#9546,#9547,#9548));
#3143=EDGE_LOOP('',(#9549,#9550,#9551,#9552));
#3144=EDGE_LOOP('',(#9553,#9554,#9555,#9556));
#3145=EDGE_LOOP('',(#9557,#9558,#9559,#9560));
#3146=EDGE_LOOP('',(#9561,#9562,#9563,#9564));
#3147=EDGE_LOOP('',(#9565));
#3148=EDGE_LOOP('',(#9566));
#3149=EDGE_LOOP('',(#9567));
#3150=EDGE_LOOP('',(#9568));
#3151=EDGE_LOOP('',(#9569));
#3152=EDGE_LOOP('',(#9570));
#3153=EDGE_LOOP('',(#9571));
#3154=EDGE_LOOP('',(#9572));
#3155=EDGE_LOOP('',(#9573));
#3156=EDGE_LOOP('',(#9574));
#3157=EDGE_LOOP('',(#9575));
#3158=EDGE_LOOP('',(#9576));
#4137=LINE('',#21054,#4812);
#4138=LINE('',#21060,#4813);
#4139=LINE('',#21066,#4814);
#4140=LINE('',#21072,#4815);
#4141=LINE('',#21078,#4816);
#4142=LINE('',#21084,#4817);
#4812=VECTOR('',#17024,0.225);
#4813=VECTOR('',#17031,0.225);
#4814=VECTOR('',#17038,0.225);
#4815=VECTOR('',#17045,0.225);
#4816=VECTOR('',#17052,1.02);
#4817=VECTOR('',#17059,2.2);
#5495=CIRCLE('',#14306,0.225);
#5496=CIRCLE('',#14307,0.225);
#5497=CIRCLE('',#14309,0.225);
#5498=CIRCLE('',#14310,0.225);
#5499=CIRCLE('',#14312,0.225);
#5500=CIRCLE('',#14313,0.225);
#5501=CIRCLE('',#14315,0.225);
#5502=CIRCLE('',#14316,0.225);
#5503=CIRCLE('',#14318,1.02);
#5504=CIRCLE('',#14319,1.02);
#5505=CIRCLE('',#14321,2.2);
#5506=CIRCLE('',#14322,2.2);
#6345=VERTEX_POINT('',#21051);
#6346=VERTEX_POINT('',#21053);
#6347=VERTEX_POINT('',#21057);
#6348=VERTEX_POINT('',#21059);
#6349=VERTEX_POINT('',#21063);
#6350=VERTEX_POINT('',#21065);
#6351=VERTEX_POINT('',#21069);
#6352=VERTEX_POINT('',#21071);
#6353=VERTEX_POINT('',#21075);
#6354=VERTEX_POINT('',#21077);
#6355=VERTEX_POINT('',#21081);
#6356=VERTEX_POINT('',#21083);
#7510=EDGE_CURVE('',#6345,#6345,#5495,.T.);
#7511=EDGE_CURVE('',#6345,#6346,#4137,.T.);
#7512=EDGE_CURVE('',#6346,#6346,#5496,.T.);
#7513=EDGE_CURVE('',#6347,#6347,#5497,.T.);
#7514=EDGE_CURVE('',#6347,#6348,#4138,.T.);
#7515=EDGE_CURVE('',#6348,#6348,#5498,.T.);
#7516=EDGE_CURVE('',#6349,#6349,#5499,.T.);
#7517=EDGE_CURVE('',#6349,#6350,#4139,.T.);
#7518=EDGE_CURVE('',#6350,#6350,#5500,.T.);
#7519=EDGE_CURVE('',#6351,#6351,#5501,.T.);
#7520=EDGE_CURVE('',#6351,#6352,#4140,.T.);
#7521=EDGE_CURVE('',#6352,#6352,#5502,.T.);
#7522=EDGE_CURVE('',#6353,#6353,#5503,.T.);
#7523=EDGE_CURVE('',#6353,#6354,#4141,.T.);
#7524=EDGE_CURVE('',#6354,#6354,#5504,.T.);
#7525=EDGE_CURVE('',#6355,#6355,#5505,.T.);
#7526=EDGE_CURVE('',#6355,#6356,#4142,.T.);
#7527=EDGE_CURVE('',#6356,#6356,#5506,.T.);
#9541=ORIENTED_EDGE('',*,*,#7510,.F.);
#9542=ORIENTED_EDGE('',*,*,#7511,.T.);
#9543=ORIENTED_EDGE('',*,*,#7512,.F.);
#9544=ORIENTED_EDGE('',*,*,#7511,.F.);
#9545=ORIENTED_EDGE('',*,*,#7513,.F.);
#9546=ORIENTED_EDGE('',*,*,#7514,.T.);
#9547=ORIENTED_EDGE('',*,*,#7515,.F.);
#9548=ORIENTED_EDGE('',*,*,#7514,.F.);
#9549=ORIENTED_EDGE('',*,*,#7516,.F.);
#9550=ORIENTED_EDGE('',*,*,#7517,.T.);
#9551=ORIENTED_EDGE('',*,*,#7518,.F.);
#9552=ORIENTED_EDGE('',*,*,#7517,.F.);
#9553=ORIENTED_EDGE('',*,*,#7519,.F.);
#9554=ORIENTED_EDGE('',*,*,#7520,.T.);
#9555=ORIENTED_EDGE('',*,*,#7521,.F.);
#9556=ORIENTED_EDGE('',*,*,#7520,.F.);
#9557=ORIENTED_EDGE('',*,*,#7522,.F.);
#9558=ORIENTED_EDGE('',*,*,#7523,.T.);
#9559=ORIENTED_EDGE('',*,*,#7524,.T.);
#9560=ORIENTED_EDGE('',*,*,#7523,.F.);
#9561=ORIENTED_EDGE('',*,*,#7525,.F.);
#9562=ORIENTED_EDGE('',*,*,#7526,.T.);
#9563=ORIENTED_EDGE('',*,*,#7527,.T.);
#9564=ORIENTED_EDGE('',*,*,#7526,.F.);
#9565=ORIENTED_EDGE('',*,*,#7525,.T.);
#9566=ORIENTED_EDGE('',*,*,#7522,.T.);
#9567=ORIENTED_EDGE('',*,*,#7521,.T.);
#9568=ORIENTED_EDGE('',*,*,#7518,.T.);
#9569=ORIENTED_EDGE('',*,*,#7515,.T.);
#9570=ORIENTED_EDGE('',*,*,#7512,.T.);
#9571=ORIENTED_EDGE('',*,*,#7527,.F.);
#9572=ORIENTED_EDGE('',*,*,#7524,.F.);
#9573=ORIENTED_EDGE('',*,*,#7519,.T.);
#9574=ORIENTED_EDGE('',*,*,#7516,.T.);
#9575=ORIENTED_EDGE('',*,*,#7513,.T.);
#9576=ORIENTED_EDGE('',*,*,#7510,.T.);
#11413=CYLINDRICAL_SURFACE('',#14305,0.225);
#11414=CYLINDRICAL_SURFACE('',#14308,0.225);
#11415=CYLINDRICAL_SURFACE('',#14311,0.225);
#11416=CYLINDRICAL_SURFACE('',#14314,0.225);
#11417=CYLINDRICAL_SURFACE('',#14317,1.02);
#11418=CYLINDRICAL_SURFACE('',#14320,2.2);
#11908=ADVANCED_FACE('',(#2183),#11413,.F.);
#11909=ADVANCED_FACE('',(#2184),#11414,.F.);
#11910=ADVANCED_FACE('',(#2185),#11415,.F.);
#11911=ADVANCED_FACE('',(#2186),#11416,.F.);
#11912=ADVANCED_FACE('',(#2187),#11417,.F.);
#11913=ADVANCED_FACE('',(#2188),#11418,.T.);
#11914=ADVANCED_FACE('',(#2189,#1268,#1269,#1270,#1271,#1272),#1635,.T.);
#11915=ADVANCED_FACE('',(#2190,#1273,#1274,#1275,#1276,#1277),#1636,.F.);
#12429=CLOSED_SHELL('',(#11908,#11909,#11910,#11911,#11912,#11913,#11914,
#11915));
#14304=AXIS2_PLACEMENT_3D('',#21049,#17018,#17019);
#14305=AXIS2_PLACEMENT_3D('',#21050,#17020,#17021);
#14306=AXIS2_PLACEMENT_3D('',#21052,#17022,#17023);
#14307=AXIS2_PLACEMENT_3D('',#21055,#17025,#17026);
#14308=AXIS2_PLACEMENT_3D('',#21056,#17027,#17028);
#14309=AXIS2_PLACEMENT_3D('',#21058,#17029,#17030);
#14310=AXIS2_PLACEMENT_3D('',#21061,#17032,#17033);
#14311=AXIS2_PLACEMENT_3D('',#21062,#17034,#17035);
#14312=AXIS2_PLACEMENT_3D('',#21064,#17036,#17037);
#14313=AXIS2_PLACEMENT_3D('',#21067,#17039,#17040);
#14314=AXIS2_PLACEMENT_3D('',#21068,#17041,#17042);
#14315=AXIS2_PLACEMENT_3D('',#21070,#17043,#17044);
#14316=AXIS2_PLACEMENT_3D('',#21073,#17046,#17047);
#14317=AXIS2_PLACEMENT_3D('',#21074,#17048,#17049);
#14318=AXIS2_PLACEMENT_3D('',#21076,#17050,#17051);
#14319=AXIS2_PLACEMENT_3D('',#21079,#17053,#17054);
#14320=AXIS2_PLACEMENT_3D('',#21080,#17055,#17056);
#14321=AXIS2_PLACEMENT_3D('',#21082,#17057,#17058);
#14322=AXIS2_PLACEMENT_3D('',#21085,#17060,#17061);
#14323=AXIS2_PLACEMENT_3D('',#21086,#17062,#17063);
#14324=AXIS2_PLACEMENT_3D('',#21087,#17064,#17065);
#17018=DIRECTION('axis',(0.,0.,1.));
#17019=DIRECTION('refdir',(1.,0.,0.));
#17020=DIRECTION('center_axis',(0.,1.,0.));
#17021=DIRECTION('ref_axis',(1.,0.,0.));
#17022=DIRECTION('center_axis',(0.,1.,0.));
#17023=DIRECTION('ref_axis',(1.,0.,0.));
#17024=DIRECTION('',(0.,1.,0.));
#17025=DIRECTION('center_axis',(0.,-1.,0.));
#17026=DIRECTION('ref_axis',(1.,0.,0.));
#17027=DIRECTION('center_axis',(0.,1.,0.));
#17028=DIRECTION('ref_axis',(1.,0.,0.));
#17029=DIRECTION('center_axis',(0.,1.,0.));
#17030=DIRECTION('ref_axis',(1.,0.,0.));
#17031=DIRECTION('',(0.,1.,0.));
#17032=DIRECTION('center_axis',(0.,-1.,0.));
#17033=DIRECTION('ref_axis',(1.,0.,0.));
#17034=DIRECTION('center_axis',(0.,1.,0.));
#17035=DIRECTION('ref_axis',(1.,0.,0.));
#17036=DIRECTION('center_axis',(0.,1.,0.));
#17037=DIRECTION('ref_axis',(1.,0.,0.));
#17038=DIRECTION('',(0.,1.,0.));
#17039=DIRECTION('center_axis',(0.,-1.,0.));
#17040=DIRECTION('ref_axis',(1.,0.,0.));
#17041=DIRECTION('center_axis',(0.,1.,0.));
#17042=DIRECTION('ref_axis',(1.,0.,0.));
#17043=DIRECTION('center_axis',(0.,1.,0.));
#17044=DIRECTION('ref_axis',(1.,0.,0.));
#17045=DIRECTION('',(0.,1.,0.));
#17046=DIRECTION('center_axis',(0.,-1.,0.));
#17047=DIRECTION('ref_axis',(1.,0.,0.));
#17048=DIRECTION('center_axis',(0.,1.,0.));
#17049=DIRECTION('ref_axis',(1.,0.,0.));
#17050=DIRECTION('center_axis',(0.,-1.,0.));
#17051=DIRECTION('ref_axis',(1.,0.,0.));
#17052=DIRECTION('',(0.,-1.,0.));
#17053=DIRECTION('center_axis',(0.,-1.,0.));
#17054=DIRECTION('ref_axis',(1.,0.,0.));
#17055=DIRECTION('center_axis',(0.,1.,0.));
#17056=DIRECTION('ref_axis',(1.,0.,0.));
#17057=DIRECTION('center_axis',(0.,1.,0.));
#17058=DIRECTION('ref_axis',(1.,0.,0.));
#17059=DIRECTION('',(0.,-1.,0.));
#17060=DIRECTION('center_axis',(0.,1.,0.));
#17061=DIRECTION('ref_axis',(1.,0.,0.));
#17062=DIRECTION('center_axis',(0.,1.,0.));
#17063=DIRECTION('ref_axis',(1.,0.,0.));
#17064=DIRECTION('center_axis',(0.,1.,0.));
#17065=DIRECTION('ref_axis',(1.,0.,0.));
#21049=CARTESIAN_POINT('',(0.,0.,0.));
#21050=CARTESIAN_POINT('Origin',(-1.30814754519511,0.4,13.6918524548049));
#21051=CARTESIAN_POINT('',(-1.53314754519511,0.5,13.6918524548049));
#21052=CARTESIAN_POINT('Origin',(-1.30814754519511,0.5,13.6918524548049));
#21053=CARTESIAN_POINT('',(-1.53314754519511,0.8,13.6918524548049));
#21054=CARTESIAN_POINT('',(-1.53314754519511,0.4,13.6918524548049));
#21055=CARTESIAN_POINT('Origin',(-1.30814754519511,0.8,13.6918524548049));
#21056=CARTESIAN_POINT('Origin',(-1.30814754519511,0.4,16.3081475451951));
#21057=CARTESIAN_POINT('',(-1.53314754519511,0.5,16.3081475451951));
#21058=CARTESIAN_POINT('Origin',(-1.30814754519511,0.5,16.3081475451951));
#21059=CARTESIAN_POINT('',(-1.53314754519511,0.8,16.3081475451951));
#21060=CARTESIAN_POINT('',(-1.53314754519511,0.4,16.3081475451951));
#21061=CARTESIAN_POINT('Origin',(-1.30814754519511,0.8,16.3081475451951));
#21062=CARTESIAN_POINT('Origin',(1.30814754519511,0.4,16.3081475451951));
#21063=CARTESIAN_POINT('',(1.08314754519511,0.5,16.3081475451951));
#21064=CARTESIAN_POINT('Origin',(1.30814754519511,0.5,16.3081475451951));
#21065=CARTESIAN_POINT('',(1.08314754519511,0.8,16.3081475451951));
#21066=CARTESIAN_POINT('',(1.08314754519511,0.4,16.3081475451951));
#21067=CARTESIAN_POINT('Origin',(1.30814754519511,0.8,16.3081475451951));
#21068=CARTESIAN_POINT('Origin',(1.30814754519511,0.4,13.6918524548049));
#21069=CARTESIAN_POINT('',(1.08314754519511,0.5,13.6918524548049));
#21070=CARTESIAN_POINT('Origin',(1.30814754519511,0.5,13.6918524548049));
#21071=CARTESIAN_POINT('',(1.08314754519511,0.8,13.6918524548049));
#21072=CARTESIAN_POINT('',(1.08314754519511,0.4,13.6918524548049));
#21073=CARTESIAN_POINT('Origin',(1.30814754519511,0.8,13.6918524548049));
#21074=CARTESIAN_POINT('Origin',(0.,0.5,15.));
#21075=CARTESIAN_POINT('',(-1.02,0.8,15.));
#21076=CARTESIAN_POINT('Origin',(0.,0.8,15.));
#21077=CARTESIAN_POINT('',(-1.02,0.5,15.));
#21078=CARTESIAN_POINT('',(-1.02,0.5,15.));
#21079=CARTESIAN_POINT('Origin',(0.,0.5,15.));
#21080=CARTESIAN_POINT('Origin',(0.,0.5,15.));
#21081=CARTESIAN_POINT('',(-2.2,0.8,15.));
#21082=CARTESIAN_POINT('Origin',(0.,0.8,15.));
#21083=CARTESIAN_POINT('',(-2.2,0.5,15.));
#21084=CARTESIAN_POINT('',(-2.2,0.5,15.));
#21085=CARTESIAN_POINT('Origin',(0.,0.5,15.));
#21086=CARTESIAN_POINT('Origin',(0.,0.8,15.));
#21087=CARTESIAN_POINT('Origin',(0.,0.5,15.));
#23534=UNCERTAINTY_MEASURE_WITH_UNIT(LENGTH_MEASURE(0.001),#23729,
'DISTANCE_ACCURACY_VALUE',
'Maximum model space distance between geometric entities at asserted c
onnectivities');
#23611=UNCERTAINTY_MEASURE_WITH_UNIT(LENGTH_MEASURE(0.001),#23729,
'DISTANCE_ACCURACY_VALUE',
'Maximum model space distance between geometric entities at asserted c
onnectivities');
#23651=(
GEOMETRIC_REPRESENTATION_CONTEXT(3)
GLOBAL_UNCERTAINTY_ASSIGNED_CONTEXT((#23534))
GLOBAL_UNIT_ASSIGNED_CONTEXT((#23729,#23731,#23732))
REPRESENTATION_CONTEXT('','3D')
);
#23728=(
GEOMETRIC_REPRESENTATION_CONTEXT(3)
GLOBAL_UNCERTAINTY_ASSIGNED_CONTEXT((#23611))
GLOBAL_UNIT_ASSIGNED_CONTEXT((#23729,#23731,#23732))
REPRESENTATION_CONTEXT('','3D')
);
#23729=(
LENGTH_UNIT()
NAMED_UNIT(*)
SI_UNIT(.CENTI.,.METRE.)
);
#23731=(
NAMED_UNIT(*)
PLANE_ANGLE_UNIT()
SI_UNIT($,.RADIAN.)
);
#23732=(
NAMED_UNIT(*)
SI_UNIT($,.STERADIAN.)
SOLID_ANGLE_UNIT()
);
#23772=SHAPE_DEFINITION_REPRESENTATION(#23888,#24151);
#23888=PRODUCT_DEFINITION_SHAPE('',$,#24268);
#24151=SHAPE_REPRESENTATION('',(#14304),#23651);
#24228=PRODUCT_DEFINITION_CONTEXT('part definition',#24578,'design');
#24268=PRODUCT_DEFINITION('Bearing cap (1)','Bearing cap (1)',#24384,#24228);
#24384=PRODUCT_DEFINITION_FORMATION('',$,#24619);
#24578=APPLICATION_CONTEXT(
'Core Data for Automotive Mechanical Design Process');
#24579=PRODUCT_CONTEXT('part definition',#24578,'mechanical');
#24619=PRODUCT('Bearing cap (1)','Bearing cap (1)','Bearing cap (1)',(#24579));
#24759=COLOUR_RGB('Grey',0.48,0.52,0.57);
#24760=FILL_AREA_STYLE_COLOUR('',#24759);
#24761=FILL_AREA_STYLE('',(#24760));
#24762=SURFACE_STYLE_FILL_AREA(#24761);
#24763=SURFACE_SIDE_STYLE('',(#24762));
#24764=SURFACE_STYLE_USAGE(.BOTH.,#24763);
#24765=PRESENTATION_STYLE_ASSIGNMENT((#24764));
ENDSEC;
END-ISO-10303-21;
